ISO-10303-21;
HEADER;
/* Generated by software containing ST-Developer
 * from STEP Tools, Inc. (www.steptools.com) 
 */

FILE_DESCRIPTION(
/* description */ ('PAT-015'),
/* implementation_level */ '2;1');

FILE_NAME(
/* name */ 'Adjuster spring shoe.step',
/* time_stamp */ '2026-10-29T16:03:43-07:00',
/* author */ (''),
/* organization */ (''),
/* preprocessor_version */ 'ST-DEVELOPER v20.2',
/* originating_system */ 'Autodesk Translation Framework v15.17.0.0',
/* authorisation */ '');

FILE_SCHEMA (('AUTOMOTIVE_DESIGN { 1 0 10303 214 3 1 1 }'));
ENDSEC;

DATA;
#10=MECHANICAL_DESIGN_GEOMETRIC_PRESENTATION_REPRESENTATION('',(#245),#10266);
#197=SHAPE_REPRESENTATION_RELATIONSHIP('SRR','None',#10368,#220);
#220=ADVANCED_BREP_SHAPE_REPRESENTATION('',(#270),#10256);
#245=STYLED_ITEM('',(#10547),#270);
#270=MANIFOLD_SOLID_BREP('Body1',#4704);
#406=FACE_BOUND('',#1172,.T.);
#515=PLANE('',#5386);
#516=PLANE('',#5390);
#517=PLANE('',#5391);
#770=FACE_OUTER_BOUND('',#1167,.T.);
#771=FACE_OUTER_BOUND('',#1168,.T.);
#772=FACE_OUTER_BOUND('',#1169,.T.);
#773=FACE_OUTER_BOUND('',#1170,.T.);
#774=FACE_OUTER_BOUND('',#1171,.T.);
#1167=EDGE_LOOP('',(#3969,#3970,#3971,#3972));
#1168=EDGE_LOOP('',(#3973));
#1169=EDGE_LOOP('',(#3974,#3975,#3976,#3977));
#1170=EDGE_LOOP('',(#3978));
#1171=EDGE_LOOP('',(#3979));
#1172=EDGE_LOOP('',(#3980));
#1502=LINE('',#9754,#1782);
#1503=LINE('',#9761,#1783);
#1782=VECTOR('',#6565,0.6);
#1783=VECTOR('',#6574,1.2);
#2069=CIRCLE('',#5384,0.6);
#2070=CIRCLE('',#5385,0.6);
#2071=CIRCLE('',#5388,1.2);
#2072=CIRCLE('',#5389,1.2);
#2403=VERTEX_POINT('',#9751);
#2404=VERTEX_POINT('',#9753);
#2405=VERTEX_POINT('',#9758);
#2406=VERTEX_POINT('',#9760);
#2940=EDGE_CURVE('',#2403,#2403,#2069,.T.);
#2941=EDGE_CURVE('',#2403,#2404,#1502,.T.);
#2942=EDGE_CURVE('',#2404,#2404,#2070,.T.);
#2943=EDGE_CURVE('',#2405,#2405,#2071,.T.);
#2944=EDGE_CURVE('',#2405,#2406,#1503,.T.);
#2945=EDGE_CURVE('',#2406,#2406,#2072,.T.);
#3969=ORIENTED_EDGE('',*,*,#2940,.F.);
#3970=ORIENTED_EDGE('',*,*,#2941,.T.);
#3971=ORIENTED_EDGE('',*,*,#2942,.T.);
#3972=ORIENTED_EDGE('',*,*,#2941,.F.);
#3973=ORIENTED_EDGE('',*,*,#2942,.F.);
#3974=ORIENTED_EDGE('',*,*,#2943,.F.);
#3975=ORIENTED_EDGE('',*,*,#2944,.T.);
#3976=ORIENTED_EDGE('',*,*,#2945,.T.);
#3977=ORIENTED_EDGE('',*,*,#2944,.F.);
#3978=ORIENTED_EDGE('',*,*,#2943,.T.);
#3979=ORIENTED_EDGE('',*,*,#2945,.F.);
#3980=ORIENTED_EDGE('',*,*,#2940,.T.);
#4391=CYLINDRICAL_SURFACE('',#5383,0.6);
#4392=CYLINDRICAL_SURFACE('',#5387,1.2);
#4605=ADVANCED_FACE('',(#770),#4391,.T.);
#4606=ADVANCED_FACE('',(#771),#515,.F.);
#4607=ADVANCED_FACE('',(#772),#4392,.T.);
#4608=ADVANCED_FACE('',(#773),#516,.T.);
#4609=ADVANCED_FACE('',(#774,#406),#517,.F.);
#4704=CLOSED_SHELL('',(#4605,#4606,#4607,#4608,#4609));
#5382=AXIS2_PLACEMENT_3D('',#9749,#6559,#6560);
#5383=AXIS2_PLACEMENT_3D('',#9750,#6561,#6562);
#5384=AXIS2_PLACEMENT_3D('',#9752,#6563,#6564);
#5385=AXIS2_PLACEMENT_3D('',#9755,#6566,#6567);
#5386=AXIS2_PLACEMENT_3D('',#9756,#6568,#6569);
#5387=AXIS2_PLACEMENT_3D('',#9757,#6570,#6571);
#5388=AXIS2_PLACEMENT_3D('',#9759,#6572,#6573);
#5389=AXIS2_PLACEMENT_3D('',#9762,#6575,#6576);
#5390=AXIS2_PLACEMENT_3D('',#9763,#6577,#6578);
#5391=AXIS2_PLACEMENT_3D('',#9764,#6579,#6580);
#6559=DIRECTION('axis',(0.,0.,1.));
#6560=DIRECTION('refdir',(1.,0.,0.));
#6561=DIRECTION('center_axis',(0.,0.,1.));
#6562=DIRECTION('ref_axis',(1.,0.,0.));
#6563=DIRECTION('center_axis',(0.,0.,1.));
#6564=DIRECTION('ref_axis',(1.,0.,0.));
#6565=DIRECTION('',(0.,0.,-1.));
#6566=DIRECTION('center_axis',(0.,0.,1.));
#6567=DIRECTION('ref_axis',(1.,0.,0.));
#6568=DIRECTION('center_axis',(0.,0.,1.));
#6569=DIRECTION('ref_axis',(1.,0.,0.));
#6570=DIRECTION('center_axis',(0.,0.,1.));
#6571=DIRECTION('ref_axis',(1.,0.,0.));
#6572=DIRECTION('center_axis',(0.,0.,1.));
#6573=DIRECTION('ref_axis',(1.,0.,0.));
#6574=DIRECTION('',(0.,0.,-1.));
#6575=DIRECTION('center_axis',(0.,0.,1.));
#6576=DIRECTION('ref_axis',(1.,0.,0.));
#6577=DIRECTION('center_axis',(0.,0.,1.));
#6578=DIRECTION('ref_axis',(1.,0.,0.));
#6579=DIRECTION('center_axis',(0.,0.,1.));
#6580=DIRECTION('ref_axis',(1.,0.,0.));
#9749=CARTESIAN_POINT('',(0.,0.,0.));
#9750=CARTESIAN_POINT('Origin',(0.,0.,7.2));
#9751=CARTESIAN_POINT('',(-0.6,-7.34788079488412E-17,7.6));
#9752=CARTESIAN_POINT('Origin',(0.,0.,7.6));
#9753=CARTESIAN_POINT('',(-0.6,-7.34788079488412E-17,6.8));
#9754=CARTESIAN_POINT('',(-0.6,-7.34788079488412E-17,7.2));
#9755=CARTESIAN_POINT('Origin',(0.,0.,6.8));
#9756=CARTESIAN_POINT('Origin',(0.,0.,6.8));
#9757=CARTESIAN_POINT('Origin',(0.,0.,7.6));
#9758=CARTESIAN_POINT('',(-1.2,-1.46957615897682E-16,8.));
#9759=CARTESIAN_POINT('Origin',(0.,0.,8.));
#9760=CARTESIAN_POINT('',(-1.2,-1.46957615897682E-16,7.6));
#9761=CARTESIAN_POINT('',(-1.2,-1.46957615897682E-16,7.6));
#9762=CARTESIAN_POINT('Origin',(0.,0.,7.6));
#9763=CARTESIAN_POINT('Origin',(0.,0.,8.));
#9764=CARTESIAN_POINT('Origin',(0.,0.,7.6));
#10231=UNCERTAINTY_MEASURE_WITH_UNIT(LENGTH_MEASURE(0.001),#10267,
'DISTANCE_ACCURACY_VALUE',
'Maximum model space distance between geometric entities at asserted c
onnectivities');
#10241=UNCERTAINTY_MEASURE_WITH_UNIT(LENGTH_MEASURE(0.001),#10267,
'DISTANCE_ACCURACY_VALUE',
'Maximum model space distance between geometric entities at asserted c
onnectivities');
#10256=(
GEOMETRIC_REPRESENTATION_CONTEXT(3)
GLOBAL_UNCERTAINTY_ASSIGNED_CONTEXT((#10231))
GLOBAL_UNIT_ASSIGNED_CONTEXT((#10267,#10269,#10270))
REPRESENTATION_CONTEXT('','3D')
);
#10266=(
GEOMETRIC_REPRESENTATION_CONTEXT(3)
GLOBAL_UNCERTAINTY_ASSIGNED_CONTEXT((#10241))
GLOBAL_UNIT_ASSIGNED_CONTEXT((#10267,#10269,#10270))
REPRESENTATION_CONTEXT('','3D')
);
#10267=(
LENGTH_UNIT()
NAMED_UNIT(*)
SI_UNIT(.CENTI.,.METRE.)
);
#10269=(
NAMED_UNIT(*)
PLANE_ANGLE_UNIT()
SI_UNIT($,.RADIAN.)
);
#10270=(
NAMED_UNIT(*)
SI_UNIT($,.STERADIAN.)
SOLID_ANGLE_UNIT()
);
#10285=SHAPE_DEFINITION_REPRESENTATION(#10309,#10368);
#10309=PRODUCT_DEFINITION_SHAPE('',$,#10393);
#10368=SHAPE_REPRESENTATION('',(#5382),#10256);
#10378=PRODUCT_DEFINITION_CONTEXT('part definition',#10452,'design');
#10393=PRODUCT_DEFINITION('Adjuster spring shoe',
'Adjuster spring shoe',#10417,#10378);
#10417=PRODUCT_DEFINITION_FORMATION('',$,#10468);
#10452=APPLICATION_CONTEXT(
'Core Data for Automotive Mechanical Design Process');
#10453=PRODUCT_CONTEXT('part definition',#10452,'mechanical');
#10468=PRODUCT('Adjuster spring shoe','Adjuster spring shoe',
'Adjuster spring shoe',(#10453));
#10541=COLOUR_RGB('Grey',0.48,0.52,0.57);
#10542=FILL_AREA_STYLE_COLOUR('',#10541);
#10543=FILL_AREA_STYLE('',(#10542));
#10544=SURFACE_STYLE_FILL_AREA(#10543);
#10545=SURFACE_SIDE_STYLE('',(#10544));
#10546=SURFACE_STYLE_USAGE(.BOTH.,#10545);
#10547=PRESENTATION_STYLE_ASSIGNMENT((#10546));
ENDSEC;
END-ISO-10303-21;
